ISO-10303-21;
HEADER;
/* Generated by software containing ST-Developer
 * from STEP Tools, Inc. (www.steptools.com) 
 */

FILE_DESCRIPTION(
/* description */ (''),
/* implementation_level */ '2;1');

FILE_NAME(
/* name */ 'Motor (1).step',
/* time_stamp */ '2026-10-22T15:07:41+06:00',
/* author */ (''),
/* organization */ (''),
/* preprocessor_version */ 'ST-DEVELOPER v20.2',
/* originating_system */ 'Autodesk Translation Framework v15.15.0.0',
/* authorisation */ '');

FILE_SCHEMA (('AUTOMOTIVE_DESIGN { 1 0 10303 214 3 1 1 }'));
ENDSEC;

DATA;
#10=MECHANICAL_DESIGN_GEOMETRIC_PRESENTATION_REPRESENTATION('',(#2876,#2877,#2878),#19220);
#67=SHAPE_REPRESENTATION_RELATIONSHIP('SRR','None',#19270,#81);
#81=ADVANCED_BREP_SHAPE_REPRESENTATION('',(#95),#19206);
#95=MANIFOLD_SOLID_BREP('Motor',#11314);
#109=FACE_BOUND('',#3450,.T.);
#626=PLANE('',#11493);
#627=PLANE('',#11507);
#628=PLANE('',#11519);
#839=LINE('',#16085,#1694);
#840=LINE('',#16106,#1695);
#841=LINE('',#16115,#1696);
#842=LINE('',#16127,#1697);
#1694=VECTOR('',#12744,21.2480593298244);
#1695=VECTOR('',#12771,21.2480593298244);
#1696=VECTOR('',#12784,6.);
#1697=VECTOR('',#12799,21.2480593298244);
#2549=CYLINDRICAL_SURFACE('',#11490,21.2480593298244);
#2550=CYLINDRICAL_SURFACE('',#11502,21.2480593298244);
#2551=CYLINDRICAL_SURFACE('',#11509,6.);
#2552=CYLINDRICAL_SURFACE('',#11516,21.2480593298244);
#2876=STYLED_ITEM('',(#19417),#10769);
#2877=STYLED_ITEM('',(#19417),#10773);
#2878=STYLED_ITEM('',(#19417),#95);
#2892=FACE_OUTER_BOUND('',#3438,.T.);
#2893=FACE_OUTER_BOUND('',#3439,.T.);
#2894=FACE_OUTER_BOUND('',#3440,.T.);
#2895=FACE_OUTER_BOUND('',#3441,.T.);
#2896=FACE_OUTER_BOUND('',#3442,.T.);
#2897=FACE_OUTER_BOUND('',#3443,.T.);
#2898=FACE_OUTER_BOUND('',#3444,.T.);
#2899=FACE_OUTER_BOUND('',#3445,.T.);
#2900=FACE_OUTER_BOUND('',#3446,.T.);
#2901=FACE_OUTER_BOUND('',#3447,.T.);
#2902=FACE_OUTER_BOUND('',#3448,.T.);
#2903=FACE_OUTER_BOUND('',#3449,.T.);
#2904=FACE_OUTER_BOUND('',#3451,.T.);
#3438=EDGE_LOOP('',(#7712,#7713,#7714,#7715,#7716));
#3439=EDGE_LOOP('',(#7717,#7718,#7719,#7720,#7721,#7722));
#3440=EDGE_LOOP('',(#7723));
#3441=EDGE_LOOP('',(#7724,#7725,#7726,#7727,#7728));
#3442=EDGE_LOOP('',(#7729,#7730,#7731,#7732,#7733));
#3443=EDGE_LOOP('',(#7734,#7735,#7736,#7737,#7738,#7739));
#3444=EDGE_LOOP('',(#7740,#7741,#7742,#7743,#7744));
#3445=EDGE_LOOP('',(#7745));
#3446=EDGE_LOOP('',(#7746,#7747,#7748,#7749));
#3447=EDGE_LOOP('',(#7750,#7751,#7752,#7753,#7754));
#3448=EDGE_LOOP('',(#7755,#7756,#7757,#7758,#7759,#7760));
#3449=EDGE_LOOP('',(#7761));
#3450=EDGE_LOOP('',(#7762));
#3451=EDGE_LOOP('',(#7763,#7764,#7765,#7766,#7767));
#4501=CIRCLE('',#11486,20.7480593298244);
#4502=CIRCLE('',#11487,0.5);
#4503=CIRCLE('',#11488,21.2480593298244);
#4504=CIRCLE('',#11489,21.2480593298244);
#4505=CIRCLE('',#11491,21.2480593298244);
#4506=CIRCLE('',#11492,21.2480593298244);
#4507=CIRCLE('',#11495,0.5);
#4508=CIRCLE('',#11496,20.7480593298244);
#4509=CIRCLE('',#11498,21.2480593298244);
#4510=CIRCLE('',#11499,0.5);
#4511=CIRCLE('',#11500,20.7480593298244);
#4512=CIRCLE('',#11501,21.2480593298244);
#4513=CIRCLE('',#11503,21.2480593298244);
#4514=CIRCLE('',#11504,21.2480593298244);
#4515=CIRCLE('',#11506,0.5);
#4516=CIRCLE('',#11508,6.);
#4517=CIRCLE('',#11510,6.);
#4518=CIRCLE('',#11512,20.7480593298244);
#4519=CIRCLE('',#11513,0.5);
#4520=CIRCLE('',#11514,21.2480593298244);
#4521=CIRCLE('',#11515,21.2480593298244);
#4522=CIRCLE('',#11517,21.2480593298244);
#4523=CIRCLE('',#11518,21.2480593298244);
#4524=CIRCLE('',#11521,0.5);
#5171=VERTEX_POINT('',#16076);
#5172=VERTEX_POINT('',#16078);
#5173=VERTEX_POINT('',#16080);
#5174=VERTEX_POINT('',#16084);
#5175=VERTEX_POINT('',#16086);
#5176=VERTEX_POINT('',#16091);
#5177=VERTEX_POINT('',#16095);
#5178=VERTEX_POINT('',#16096);
#5179=VERTEX_POINT('',#16098);
#5180=VERTEX_POINT('',#16103);
#5181=VERTEX_POINT('',#16104);
#5182=VERTEX_POINT('',#16111);
#5183=VERTEX_POINT('',#16114);
#5184=VERTEX_POINT('',#16118);
#5185=VERTEX_POINT('',#16120);
#5186=VERTEX_POINT('',#16122);
#5187=VERTEX_POINT('',#16126);
#5188=VERTEX_POINT('',#16128);
#6187=EDGE_CURVE('',#5171,#5171,#4501,.T.);
#6188=EDGE_CURVE('',#5171,#5172,#4502,.T.);
#6189=EDGE_CURVE('',#5172,#5173,#4503,.T.);
#6190=EDGE_CURVE('',#5173,#5172,#4504,.T.);
#6191=EDGE_CURVE('',#5173,#5174,#839,.T.);
#6192=EDGE_CURVE('',#5175,#5174,#4505,.T.);
#6193=EDGE_CURVE('',#5174,#5175,#4506,.T.);
#6194=EDGE_CURVE('',#5175,#5176,#4507,.T.);
#6195=EDGE_CURVE('',#5176,#5176,#4508,.T.);
#6196=EDGE_CURVE('',#5177,#5178,#4509,.T.);
#6197=EDGE_CURVE('',#5178,#5179,#4510,.T.);
#6198=EDGE_CURVE('',#5179,#5179,#4511,.T.);
#6199=EDGE_CURVE('',#5178,#5177,#4512,.T.);
#6200=EDGE_CURVE('',#5180,#5181,#4513,.T.);
#6201=EDGE_CURVE('',#5180,#5177,#840,.T.);
#6202=EDGE_CURVE('',#5181,#5180,#4514,.T.);
#6203=EDGE_CURVE('',#5176,#5181,#4515,.T.);
#6204=EDGE_CURVE('',#5182,#5182,#4516,.T.);
#6205=EDGE_CURVE('',#5182,#5183,#841,.T.);
#6206=EDGE_CURVE('',#5183,#5183,#4517,.T.);
#6207=EDGE_CURVE('',#5184,#5184,#4518,.T.);
#6208=EDGE_CURVE('',#5184,#5185,#4519,.T.);
#6209=EDGE_CURVE('',#5185,#5186,#4520,.T.);
#6210=EDGE_CURVE('',#5186,#5185,#4521,.T.);
#6211=EDGE_CURVE('',#5186,#5187,#842,.T.);
#6212=EDGE_CURVE('',#5188,#5187,#4522,.T.);
#6213=EDGE_CURVE('',#5187,#5188,#4523,.T.);
#6214=EDGE_CURVE('',#5179,#5188,#4524,.T.);
#7712=ORIENTED_EDGE('',*,*,#6187,.T.);
#7713=ORIENTED_EDGE('',*,*,#6188,.T.);
#7714=ORIENTED_EDGE('',*,*,#6189,.T.);
#7715=ORIENTED_EDGE('',*,*,#6190,.T.);
#7716=ORIENTED_EDGE('',*,*,#6188,.F.);
#7717=ORIENTED_EDGE('',*,*,#6190,.F.);
#7718=ORIENTED_EDGE('',*,*,#6191,.T.);
#7719=ORIENTED_EDGE('',*,*,#6192,.F.);
#7720=ORIENTED_EDGE('',*,*,#6193,.F.);
#7721=ORIENTED_EDGE('',*,*,#6191,.F.);
#7722=ORIENTED_EDGE('',*,*,#6189,.F.);
#7723=ORIENTED_EDGE('',*,*,#6187,.F.);
#7724=ORIENTED_EDGE('',*,*,#6193,.T.);
#7725=ORIENTED_EDGE('',*,*,#6194,.T.);
#7726=ORIENTED_EDGE('',*,*,#6195,.F.);
#7727=ORIENTED_EDGE('',*,*,#6194,.F.);
#7728=ORIENTED_EDGE('',*,*,#6192,.T.);
#7729=ORIENTED_EDGE('',*,*,#6196,.T.);
#7730=ORIENTED_EDGE('',*,*,#6197,.T.);
#7731=ORIENTED_EDGE('',*,*,#6198,.F.);
#7732=ORIENTED_EDGE('',*,*,#6197,.F.);
#7733=ORIENTED_EDGE('',*,*,#6199,.T.);
#7734=ORIENTED_EDGE('',*,*,#6200,.F.);
#7735=ORIENTED_EDGE('',*,*,#6201,.T.);
#7736=ORIENTED_EDGE('',*,*,#6199,.F.);
#7737=ORIENTED_EDGE('',*,*,#6196,.F.);
#7738=ORIENTED_EDGE('',*,*,#6201,.F.);
#7739=ORIENTED_EDGE('',*,*,#6202,.F.);
#7740=ORIENTED_EDGE('',*,*,#6195,.T.);
#7741=ORIENTED_EDGE('',*,*,#6203,.T.);
#7742=ORIENTED_EDGE('',*,*,#6202,.T.);
#7743=ORIENTED_EDGE('',*,*,#6200,.T.);
#7744=ORIENTED_EDGE('',*,*,#6203,.F.);
#7745=ORIENTED_EDGE('',*,*,#6204,.F.);
#7746=ORIENTED_EDGE('',*,*,#6204,.T.);
#7747=ORIENTED_EDGE('',*,*,#6205,.T.);
#7748=ORIENTED_EDGE('',*,*,#6206,.F.);
#7749=ORIENTED_EDGE('',*,*,#6205,.F.);
#7750=ORIENTED_EDGE('',*,*,#6207,.T.);
#7751=ORIENTED_EDGE('',*,*,#6208,.T.);
#7752=ORIENTED_EDGE('',*,*,#6209,.T.);
#7753=ORIENTED_EDGE('',*,*,#6210,.T.);
#7754=ORIENTED_EDGE('',*,*,#6208,.F.);
#7755=ORIENTED_EDGE('',*,*,#6210,.F.);
#7756=ORIENTED_EDGE('',*,*,#6211,.T.);
#7757=ORIENTED_EDGE('',*,*,#6212,.F.);
#7758=ORIENTED_EDGE('',*,*,#6213,.F.);
#7759=ORIENTED_EDGE('',*,*,#6211,.F.);
#7760=ORIENTED_EDGE('',*,*,#6209,.F.);
#7761=ORIENTED_EDGE('',*,*,#6207,.F.);
#7762=ORIENTED_EDGE('',*,*,#6206,.T.);
#7763=ORIENTED_EDGE('',*,*,#6198,.T.);
#7764=ORIENTED_EDGE('',*,*,#6214,.T.);
#7765=ORIENTED_EDGE('',*,*,#6212,.T.);
#7766=ORIENTED_EDGE('',*,*,#6213,.T.);
#7767=ORIENTED_EDGE('',*,*,#6214,.F.);
#10762=TOROIDAL_SURFACE('',#11485,20.7480593298244,0.5);
#10763=TOROIDAL_SURFACE('',#11494,20.7480593298244,0.5);
#10764=TOROIDAL_SURFACE('',#11497,20.7480593298244,0.5);
#10765=TOROIDAL_SURFACE('',#11505,20.7480593298244,0.5);
#10766=TOROIDAL_SURFACE('',#11511,20.7480593298244,0.5);
#10767=TOROIDAL_SURFACE('',#11520,20.7480593298244,0.5);
#10768=ADVANCED_FACE('',(#2892),#10762,.T.);
#10769=ADVANCED_FACE('',(#2893),#2549,.T.);
#10770=ADVANCED_FACE('',(#2894),#626,.T.);
#10771=ADVANCED_FACE('',(#2895),#10763,.T.);
#10772=ADVANCED_FACE('',(#2896),#10764,.T.);
#10773=ADVANCED_FACE('',(#2897),#2550,.T.);
#10774=ADVANCED_FACE('',(#2898),#10765,.T.);
#10775=ADVANCED_FACE('',(#2899),#627,.T.);
#10776=ADVANCED_FACE('',(#2900),#2551,.T.);
#10777=ADVANCED_FACE('',(#2901),#10766,.T.);
#10778=ADVANCED_FACE('',(#2902),#2552,.T.);
#10779=ADVANCED_FACE('',(#2903,#109),#628,.T.);
#10780=ADVANCED_FACE('',(#2904),#10767,.T.);
#11314=CLOSED_SHELL('',(#10768,#10769,#10770,#10771,#10772,#10773,#10774,
#10775,#10776,#10777,#10778,#10779,#10780));
#11484=AXIS2_PLACEMENT_3D('',#16074,#12730,#12731);
#11485=AXIS2_PLACEMENT_3D('',#16075,#12732,#12733);
#11486=AXIS2_PLACEMENT_3D('',#16077,#12734,#12735);
#11487=AXIS2_PLACEMENT_3D('',#16079,#12736,#12737);
#11488=AXIS2_PLACEMENT_3D('',#16081,#12738,#12739);
#11489=AXIS2_PLACEMENT_3D('',#16082,#12740,#12741);
#11490=AXIS2_PLACEMENT_3D('',#16083,#12742,#12743);
#11491=AXIS2_PLACEMENT_3D('',#16087,#12745,#12746);
#11492=AXIS2_PLACEMENT_3D('',#16088,#12747,#12748);
#11493=AXIS2_PLACEMENT_3D('',#16089,#12749,#12750);
#11494=AXIS2_PLACEMENT_3D('',#16090,#12751,#12752);
#11495=AXIS2_PLACEMENT_3D('',#16092,#12753,#12754);
#11496=AXIS2_PLACEMENT_3D('',#16093,#12755,#12756);
#11497=AXIS2_PLACEMENT_3D('',#16094,#12757,#12758);
#11498=AXIS2_PLACEMENT_3D('',#16097,#12759,#12760);
#11499=AXIS2_PLACEMENT_3D('',#16099,#12761,#12762);
#11500=AXIS2_PLACEMENT_3D('',#16100,#12763,#12764);
#11501=AXIS2_PLACEMENT_3D('',#16101,#12765,#12766);
#11502=AXIS2_PLACEMENT_3D('',#16102,#12767,#12768);
#11503=AXIS2_PLACEMENT_3D('',#16105,#12769,#12770);
#11504=AXIS2_PLACEMENT_3D('',#16107,#12772,#12773);
#11505=AXIS2_PLACEMENT_3D('',#16108,#12774,#12775);
#11506=AXIS2_PLACEMENT_3D('',#16109,#12776,#12777);
#11507=AXIS2_PLACEMENT_3D('',#16110,#12778,#12779);
#11508=AXIS2_PLACEMENT_3D('',#16112,#12780,#12781);
#11509=AXIS2_PLACEMENT_3D('',#16113,#12782,#12783);
#11510=AXIS2_PLACEMENT_3D('',#16116,#12785,#12786);
#11511=AXIS2_PLACEMENT_3D('',#16117,#12787,#12788);
#11512=AXIS2_PLACEMENT_3D('',#16119,#12789,#12790);
#11513=AXIS2_PLACEMENT_3D('',#16121,#12791,#12792);
#11514=AXIS2_PLACEMENT_3D('',#16123,#12793,#12794);
#11515=AXIS2_PLACEMENT_3D('',#16124,#12795,#12796);
#11516=AXIS2_PLACEMENT_3D('',#16125,#12797,#12798);
#11517=AXIS2_PLACEMENT_3D('',#16129,#12800,#12801);
#11518=AXIS2_PLACEMENT_3D('',#16130,#12802,#12803);
#11519=AXIS2_PLACEMENT_3D('',#16131,#12804,#12805);
#11520=AXIS2_PLACEMENT_3D('',#16132,#12806,#12807);
#11521=AXIS2_PLACEMENT_3D('',#16133,#12808,#12809);
#12730=DIRECTION('axis',(0.,0.,1.));
#12731=DIRECTION('refdir',(1.,0.,0.));
#12732=DIRECTION('center_axis',(0.,-1.,0.));
#12733=DIRECTION('ref_axis',(0.,0.,-1.));
#12734=DIRECTION('center_axis',(0.,1.,0.));
#12735=DIRECTION('ref_axis',(1.,0.,0.));
#12736=DIRECTION('center_axis',(-1.,0.,-2.09002244843475E-16));
#12737=DIRECTION('ref_axis',(-2.09002244843475E-16,0.,1.));
#12738=DIRECTION('center_axis',(0.,-1.,0.));
#12739=DIRECTION('ref_axis',(1.,0.,0.));
#12740=DIRECTION('center_axis',(0.,-1.,0.));
#12741=DIRECTION('ref_axis',(1.,0.,0.));
#12742=DIRECTION('center_axis',(0.,-1.,0.));
#12743=DIRECTION('ref_axis',(1.,0.,0.));
#12744=DIRECTION('',(0.,1.,0.));
#12745=DIRECTION('center_axis',(0.,1.,0.));
#12746=DIRECTION('ref_axis',(1.,0.,0.));
#12747=DIRECTION('center_axis',(0.,1.,0.));
#12748=DIRECTION('ref_axis',(1.,0.,0.));
#12749=DIRECTION('center_axis',(0.,-1.,0.));
#12750=DIRECTION('ref_axis',(1.,0.,0.));
#12751=DIRECTION('center_axis',(0.,-1.,0.));
#12752=DIRECTION('ref_axis',(0.,0.,-1.));
#12753=DIRECTION('center_axis',(-1.,0.,-2.09002244843475E-16));
#12754=DIRECTION('ref_axis',(-2.09002244843475E-16,0.,1.));
#12755=DIRECTION('center_axis',(0.,1.,0.));
#12756=DIRECTION('ref_axis',(1.,0.,0.));
#12757=DIRECTION('center_axis',(0.,-1.,0.));
#12758=DIRECTION('ref_axis',(0.,0.,-1.));
#12759=DIRECTION('center_axis',(0.,1.,0.));
#12760=DIRECTION('ref_axis',(1.,0.,0.));
#12761=DIRECTION('center_axis',(-1.,0.,-2.09002244843475E-16));
#12762=DIRECTION('ref_axis',(-2.09002244843475E-16,0.,1.));
#12763=DIRECTION('center_axis',(0.,1.,0.));
#12764=DIRECTION('ref_axis',(1.,0.,0.));
#12765=DIRECTION('center_axis',(0.,1.,0.));
#12766=DIRECTION('ref_axis',(1.,0.,0.));
#12767=DIRECTION('center_axis',(0.,-1.,0.));
#12768=DIRECTION('ref_axis',(1.,0.,0.));
#12769=DIRECTION('center_axis',(0.,-1.,0.));
#12770=DIRECTION('ref_axis',(1.,0.,0.));
#12771=DIRECTION('',(0.,1.,0.));
#12772=DIRECTION('center_axis',(0.,-1.,0.));
#12773=DIRECTION('ref_axis',(1.,0.,0.));
#12774=DIRECTION('center_axis',(0.,-1.,0.));
#12775=DIRECTION('ref_axis',(0.,0.,-1.));
#12776=DIRECTION('center_axis',(-1.,0.,-2.09002244843475E-16));
#12777=DIRECTION('ref_axis',(-2.09002244843475E-16,0.,1.));
#12778=DIRECTION('center_axis',(0.,1.,0.));
#12779=DIRECTION('ref_axis',(-1.,0.,0.));
#12780=DIRECTION('center_axis',(0.,-1.,0.));
#12781=DIRECTION('ref_axis',(-1.,0.,0.));
#12782=DIRECTION('center_axis',(0.,1.,0.));
#12783=DIRECTION('ref_axis',(-1.,0.,0.));
#12784=DIRECTION('',(0.,-1.,0.));
#12785=DIRECTION('center_axis',(0.,-1.,0.));
#12786=DIRECTION('ref_axis',(-1.,0.,0.));
#12787=DIRECTION('center_axis',(0.,1.,0.));
#12788=DIRECTION('ref_axis',(0.,0.,1.));
#12789=DIRECTION('center_axis',(0.,-1.,0.));
#12790=DIRECTION('ref_axis',(1.,0.,0.));
#12791=DIRECTION('center_axis',(-1.,0.,2.09002244843475E-16));
#12792=DIRECTION('ref_axis',(-2.09002244843475E-16,0.,-1.));
#12793=DIRECTION('center_axis',(0.,1.,0.));
#12794=DIRECTION('ref_axis',(1.,0.,0.));
#12795=DIRECTION('center_axis',(0.,1.,0.));
#12796=DIRECTION('ref_axis',(1.,0.,0.));
#12797=DIRECTION('center_axis',(0.,1.,0.));
#12798=DIRECTION('ref_axis',(1.,0.,0.));
#12799=DIRECTION('',(0.,-1.,0.));
#12800=DIRECTION('center_axis',(0.,-1.,0.));
#12801=DIRECTION('ref_axis',(1.,0.,0.));
#12802=DIRECTION('center_axis',(0.,-1.,0.));
#12803=DIRECTION('ref_axis',(1.,0.,0.));
#12804=DIRECTION('center_axis',(0.,1.,0.));
#12805=DIRECTION('ref_axis',(1.,0.,0.));
#12806=DIRECTION('center_axis',(0.,-1.,0.));
#12807=DIRECTION('ref_axis',(0.,0.,-1.));
#12808=DIRECTION('center_axis',(-1.,0.,-2.09002244843475E-16));
#12809=DIRECTION('ref_axis',(-2.09002244843475E-16,0.,1.));
#16074=CARTESIAN_POINT('',(0.,0.,0.));
#16075=CARTESIAN_POINT('Origin',(24.1201056133058,-79.5,35.8480593298244));
#16076=CARTESIAN_POINT('',(24.1201056133058,-80.,56.5961186596487));
#16077=CARTESIAN_POINT('Origin',(24.1201056133058,-80.,35.8480593298244));
#16078=CARTESIAN_POINT('',(24.1201056133058,-79.5,57.0961186596487));
#16079=CARTESIAN_POINT('Origin',(24.1201056133058,-79.5,56.5961186596487));
#16080=CARTESIAN_POINT('',(2.87204628348146,-79.5,35.8480593298243));
#16081=CARTESIAN_POINT('Origin',(24.1201056133058,-79.5,35.8480593298244));
#16082=CARTESIAN_POINT('Origin',(24.1201056133058,-79.5,35.8480593298244));
#16083=CARTESIAN_POINT('Origin',(24.1201056133058,-55.,35.8480593298244));
#16084=CARTESIAN_POINT('',(2.87204628348146,-55.5,35.8480593298244));
#16085=CARTESIAN_POINT('',(2.87204628348146,-55.,35.8480593298243));
#16086=CARTESIAN_POINT('',(24.1201056133058,-55.5,57.0961186596487));
#16087=CARTESIAN_POINT('Origin',(24.1201056133058,-55.5,35.8480593298244));
#16088=CARTESIAN_POINT('Origin',(24.1201056133058,-55.5,35.8480593298244));
#16089=CARTESIAN_POINT('Origin',(24.1201056133058,-80.,35.8480593298243));
#16090=CARTESIAN_POINT('Origin',(24.1201056133058,-55.5,35.8480593298244));
#16091=CARTESIAN_POINT('',(24.1201056133058,-55.,56.5961186596487));
#16092=CARTESIAN_POINT('Origin',(24.1201056133058,-55.5,56.5961186596487));
#16093=CARTESIAN_POINT('Origin',(24.1201056133058,-55.,35.8480593298244));
#16094=CARTESIAN_POINT('Origin',(24.1201056133058,4.5,35.8480593298244));
#16095=CARTESIAN_POINT('',(2.87204628348146,4.5,35.8480593298244));
#16096=CARTESIAN_POINT('',(24.1201056133058,4.5,57.0961186596487));
#16097=CARTESIAN_POINT('Origin',(24.1201056133058,4.5,35.8480593298244));
#16098=CARTESIAN_POINT('',(24.1201056133058,5.,56.5961186596487));
#16099=CARTESIAN_POINT('Origin',(24.1201056133058,4.5,56.5961186596487));
#16100=CARTESIAN_POINT('Origin',(24.1201056133058,5.,35.8480593298244));
#16101=CARTESIAN_POINT('Origin',(24.1201056133058,4.5,35.8480593298244));
#16102=CARTESIAN_POINT('Origin',(24.1201056133058,5.,35.8480593298244));
#16103=CARTESIAN_POINT('',(2.87204628348146,-54.5,35.8480593298243));
#16104=CARTESIAN_POINT('',(24.1201056133058,-54.5,57.0961186596487));
#16105=CARTESIAN_POINT('Origin',(24.1201056133058,-54.5,35.8480593298244));
#16106=CARTESIAN_POINT('',(2.87204628348146,5.,35.8480593298243));
#16107=CARTESIAN_POINT('Origin',(24.1201056133058,-54.5,35.8480593298244));
#16108=CARTESIAN_POINT('Origin',(24.1201056133058,-54.5,35.8480593298244));
#16109=CARTESIAN_POINT('Origin',(24.1201056133058,-54.5,56.5961186596487));
#16110=CARTESIAN_POINT('Origin',(24.1201056133058,65.999994278,35.8480593298244));
#16111=CARTESIAN_POINT('',(30.1201056133058,65.999994278,35.8480593298244));
#16112=CARTESIAN_POINT('Origin',(24.1201056133058,65.999994278,35.8480593298244));
#16113=CARTESIAN_POINT('Origin',(24.1201056133058,45.,35.8480593298244));
#16114=CARTESIAN_POINT('',(30.1201056133058,45.,35.8480593298244));
#16115=CARTESIAN_POINT('',(30.1201056133058,45.,35.8480593298244));
#16116=CARTESIAN_POINT('Origin',(24.1201056133058,45.,35.8480593298244));
#16117=CARTESIAN_POINT('Origin',(24.1201056133058,44.5,35.8480593298244));
#16118=CARTESIAN_POINT('',(24.1201056133058,45.,15.1));
#16119=CARTESIAN_POINT('Origin',(24.1201056133058,45.,35.8480593298244));
#16120=CARTESIAN_POINT('',(24.1201056133058,44.5,14.6));
#16121=CARTESIAN_POINT('Origin',(24.1201056133058,44.5,15.1));
#16122=CARTESIAN_POINT('',(2.87204628348146,44.5,35.8480593298244));
#16123=CARTESIAN_POINT('Origin',(24.1201056133058,44.5,35.8480593298244));
#16124=CARTESIAN_POINT('Origin',(24.1201056133058,44.5,35.8480593298244));
#16125=CARTESIAN_POINT('Origin',(24.1201056133058,25.,35.8480593298244));
#16126=CARTESIAN_POINT('',(2.87204628348146,5.5,35.8480593298243));
#16127=CARTESIAN_POINT('',(2.87204628348146,25.,35.8480593298244));
#16128=CARTESIAN_POINT('',(24.1201056133058,5.5,57.0961186596487));
#16129=CARTESIAN_POINT('Origin',(24.1201056133058,5.5,35.8480593298244));
#16130=CARTESIAN_POINT('Origin',(24.1201056133058,5.5,35.8480593298244));
#16131=CARTESIAN_POINT('Origin',(24.1201056133058,45.,35.8480593298243));
#16132=CARTESIAN_POINT('Origin',(24.1201056133058,5.5,35.8480593298244));
#16133=CARTESIAN_POINT('Origin',(24.1201056133058,5.5,56.5961186596487));
#19190=UNCERTAINTY_MEASURE_WITH_UNIT(LENGTH_MEASURE(0.01),#19221,
'DISTANCE_ACCURACY_VALUE',
'Maximum model space distance between geometric entities at asserted c
onnectivities');
#19204=UNCERTAINTY_MEASURE_WITH_UNIT(LENGTH_MEASURE(0.01),#19221,
'DISTANCE_ACCURACY_VALUE',
'Maximum model space distance between geometric entities at asserted c
onnectivities');
#19206=(
GEOMETRIC_REPRESENTATION_CONTEXT(3)
GLOBAL_UNCERTAINTY_ASSIGNED_CONTEXT((#19190))
GLOBAL_UNIT_ASSIGNED_CONTEXT((#19221,#19223,#19224))
REPRESENTATION_CONTEXT('','3D')
);
#19220=(
GEOMETRIC_REPRESENTATION_CONTEXT(3)
GLOBAL_UNCERTAINTY_ASSIGNED_CONTEXT((#19204))
GLOBAL_UNIT_ASSIGNED_CONTEXT((#19221,#19223,#19224))
REPRESENTATION_CONTEXT('','3D')
);
#19221=(
LENGTH_UNIT()
NAMED_UNIT(*)
SI_UNIT(.MILLI.,.METRE.)
);
#19223=(
NAMED_UNIT(*)
PLANE_ANGLE_UNIT()
SI_UNIT($,.RADIAN.)
);
#19224=(
NAMED_UNIT(*)
SI_UNIT($,.STERADIAN.)
SOLID_ANGLE_UNIT()
);
#19226=SHAPE_DEFINITION_REPRESENTATION(#19241,#19270);
#19241=PRODUCT_DEFINITION_SHAPE('',$,#19286);
#19270=SHAPE_REPRESENTATION('',(#11484),#19206);
#19284=PRODUCT_DEFINITION_CONTEXT('part definition',#19331,'design');
#19286=PRODUCT_DEFINITION('Motor (1)','Motor (1)',#19301,#19284);
#19301=PRODUCT_DEFINITION_FORMATION('',$,#19334);
#19331=APPLICATION_CONTEXT(
'Core Data for Automotive Mechanical Design Process');
#19332=PRODUCT_CONTEXT('part definition',#19331,'mechanical');
#19334=PRODUCT('Motor (1)','Motor (1)',$,(#19332));
#19411=COLOUR_RGB('Off White',0.89,0.88,0.83);
#19412=FILL_AREA_STYLE_COLOUR('',#19411);
#19413=FILL_AREA_STYLE('',(#19412));
#19414=SURFACE_STYLE_FILL_AREA(#19413);
#19415=SURFACE_SIDE_STYLE('',(#19414));
#19416=SURFACE_STYLE_USAGE(.BOTH.,#19415);
#19417=PRESENTATION_STYLE_ASSIGNMENT((#19416));
ENDSEC;
END-ISO-10303-21;
